ISO-10303-21;
HEADER;
/* Generated by software containing ST-Developer
 * from STEP Tools, Inc. (www.steptools.com) 
 */

FILE_DESCRIPTION(
/* description */ ('PAT-091'),
/* implementation_level */ '2;1');

FILE_NAME(
/* name */ 'M4 low-profile retaining screw.step',
/* time_stamp */ '2026-10-27T15:34:44-07:00',
/* author */ (''),
/* organization */ (''),
/* preprocessor_version */ 'ST-DEVELOPER v20.2',
/* originating_system */ 'Autodesk Translation Framework v15.17.0.0',
/* authorisation */ '');

FILE_SCHEMA (('AUTOMOTIVE_DESIGN { 1 0 10303 214 3 1 1 }'));
ENDSEC;

DATA;
#10=MECHANICAL_DESIGN_GEOMETRIC_PRESENTATION_REPRESENTATION('',(#1048),#25100);
#828=SHAPE_REPRESENTATION_RELATIONSHIP('SRR','None',#25595,#938);
#938=ADVANCED_BREP_SHAPE_REPRESENTATION('',(#1169),#25065);
#1048=STYLED_ITEM('',(#26198),#1169);
#1169=MANIFOLD_SOLID_BREP('Body1',#13328);
#1553=FACE_BOUND('',#3803,.T.);
#1960=PLANE('',#15852);
#1961=PLANE('',#15857);
#1962=PLANE('',#15860);
#2646=FACE_OUTER_BOUND('',#3802,.T.);
#2647=FACE_OUTER_BOUND('',#3804,.T.);
#2648=FACE_OUTER_BOUND('',#3805,.T.);
#2649=FACE_OUTER_BOUND('',#3806,.T.);
#2650=FACE_OUTER_BOUND('',#3807,.T.);
#3802=EDGE_LOOP('',(#11294));
#3803=EDGE_LOOP('',(#11295));
#3804=EDGE_LOOP('',(#11296,#11297,#11298,#11299));
#3805=EDGE_LOOP('',(#11300));
#3806=EDGE_LOOP('',(#11301,#11302,#11303,#11304));
#3807=EDGE_LOOP('',(#11305));
#4757=LINE('',#23707,#5497);
#4758=LINE('',#23713,#5498);
#5497=VECTOR('',#19643,0.350000000000001);
#5498=VECTOR('',#19652,0.199999999999999);
#6128=CIRCLE('',#15853,0.350000000000001);
#6129=CIRCLE('',#15854,0.199999999999999);
#6130=CIRCLE('',#15856,0.350000000000001);
#6131=CIRCLE('',#15859,0.199999999999999);
#7153=VERTEX_POINT('',#23701);
#7154=VERTEX_POINT('',#23703);
#7155=VERTEX_POINT('',#23706);
#7156=VERTEX_POINT('',#23711);
#8582=EDGE_CURVE('',#7153,#7153,#6128,.T.);
#8583=EDGE_CURVE('',#7154,#7154,#6129,.T.);
#8584=EDGE_CURVE('',#7153,#7155,#4757,.T.);
#8585=EDGE_CURVE('',#7155,#7155,#6130,.T.);
#8586=EDGE_CURVE('',#7156,#7156,#6131,.T.);
#8587=EDGE_CURVE('',#7156,#7154,#4758,.T.);
#11294=ORIENTED_EDGE('',*,*,#8582,.T.);
#11295=ORIENTED_EDGE('',*,*,#8583,.F.);
#11296=ORIENTED_EDGE('',*,*,#8582,.F.);
#11297=ORIENTED_EDGE('',*,*,#8584,.T.);
#11298=ORIENTED_EDGE('',*,*,#8585,.T.);
#11299=ORIENTED_EDGE('',*,*,#8584,.F.);
#11300=ORIENTED_EDGE('',*,*,#8585,.F.);
#11301=ORIENTED_EDGE('',*,*,#8586,.F.);
#11302=ORIENTED_EDGE('',*,*,#8587,.T.);
#11303=ORIENTED_EDGE('',*,*,#8583,.T.);
#11304=ORIENTED_EDGE('',*,*,#8587,.F.);
#11305=ORIENTED_EDGE('',*,*,#8586,.T.);
#12325=CYLINDRICAL_SURFACE('',#15855,0.350000000000001);
#12326=CYLINDRICAL_SURFACE('',#15858,0.199999999999999);
#13013=ADVANCED_FACE('',(#2646,#1553),#1960,.T.);
#13014=ADVANCED_FACE('',(#2647),#12325,.T.);
#13015=ADVANCED_FACE('',(#2648),#1961,.F.);
#13016=ADVANCED_FACE('',(#2649),#12326,.T.);
#13017=ADVANCED_FACE('',(#2650),#1962,.T.);
#13328=CLOSED_SHELL('',(#13013,#13014,#13015,#13016,#13017));
#15851=AXIS2_PLACEMENT_3D('',#23699,#19633,#19634);
#15852=AXIS2_PLACEMENT_3D('',#23700,#19635,#19636);
#15853=AXIS2_PLACEMENT_3D('',#23702,#19637,#19638);
#15854=AXIS2_PLACEMENT_3D('',#23704,#19639,#19640);
#15855=AXIS2_PLACEMENT_3D('',#23705,#19641,#19642);
#15856=AXIS2_PLACEMENT_3D('',#23708,#19644,#19645);
#15857=AXIS2_PLACEMENT_3D('',#23709,#19646,#19647);
#15858=AXIS2_PLACEMENT_3D('',#23710,#19648,#19649);
#15859=AXIS2_PLACEMENT_3D('',#23712,#19650,#19651);
#15860=AXIS2_PLACEMENT_3D('',#23714,#19653,#19654);
#19633=DIRECTION('axis',(0.,0.,1.));
#19634=DIRECTION('refdir',(1.,0.,0.));
#19635=DIRECTION('center_axis',(0.,1.,0.));
#19636=DIRECTION('ref_axis',(1.,0.,0.));
#19637=DIRECTION('center_axis',(0.,1.,0.));
#19638=DIRECTION('ref_axis',(1.,0.,0.));
#19639=DIRECTION('center_axis',(0.,1.,0.));
#19640=DIRECTION('ref_axis',(1.,0.,0.));
#19641=DIRECTION('center_axis',(0.,1.,0.));
#19642=DIRECTION('ref_axis',(1.,0.,0.));
#19643=DIRECTION('',(0.,-1.,0.));
#19644=DIRECTION('center_axis',(0.,1.,0.));
#19645=DIRECTION('ref_axis',(1.,0.,0.));
#19646=DIRECTION('center_axis',(0.,1.,0.));
#19647=DIRECTION('ref_axis',(1.,0.,0.));
#19648=DIRECTION('center_axis',(0.,1.,0.));
#19649=DIRECTION('ref_axis',(1.,0.,0.));
#19650=DIRECTION('center_axis',(0.,1.,0.));
#19651=DIRECTION('ref_axis',(1.,0.,0.));
#19652=DIRECTION('',(0.,-1.,0.));
#19653=DIRECTION('center_axis',(0.,1.,0.));
#19654=DIRECTION('ref_axis',(1.,0.,0.));
#23699=CARTESIAN_POINT('',(0.,0.,0.));
#23700=CARTESIAN_POINT('Origin',(20.6730642762322,-5.8,9.30814754519511));
#23701=CARTESIAN_POINT('',(20.3230642762322,-5.8,9.30814754519511));
#23702=CARTESIAN_POINT('Origin',(20.6730642762322,-5.8,9.30814754519511));
#23703=CARTESIAN_POINT('',(20.4730642762322,-5.8,9.30814754519511));
#23704=CARTESIAN_POINT('Origin',(20.6730642762322,-5.8,9.30814754519511));
#23705=CARTESIAN_POINT('Origin',(20.6730642762322,-5.9,9.30814754519511));
#23706=CARTESIAN_POINT('',(20.3230642762322,-5.9,9.30814754519511));
#23707=CARTESIAN_POINT('',(20.3230642762322,-5.9,9.30814754519511));
#23708=CARTESIAN_POINT('Origin',(20.6730642762322,-5.9,9.30814754519511));
#23709=CARTESIAN_POINT('Origin',(20.6730642762322,-5.9,9.30814754519511));
#23710=CARTESIAN_POINT('Origin',(20.6730642762322,-5.8,9.30814754519511));
#23711=CARTESIAN_POINT('',(20.4730642762322,-5.1,9.30814754519511));
#23712=CARTESIAN_POINT('Origin',(20.6730642762322,-5.1,9.30814754519511));
#23713=CARTESIAN_POINT('',(20.4730642762322,-5.8,9.30814754519511));
#23714=CARTESIAN_POINT('Origin',(20.6730642762322,-5.1,9.30814754519511));
#24944=UNCERTAINTY_MEASURE_WITH_UNIT(LENGTH_MEASURE(0.001),#25101,
'DISTANCE_ACCURACY_VALUE',
'Maximum model space distance between geometric entities at asserted c
onnectivities');
#24979=UNCERTAINTY_MEASURE_WITH_UNIT(LENGTH_MEASURE(0.001),#25101,
'DISTANCE_ACCURACY_VALUE',
'Maximum model space distance between geometric entities at asserted c
onnectivities');
#25065=(
GEOMETRIC_REPRESENTATION_CONTEXT(3)
GLOBAL_UNCERTAINTY_ASSIGNED_CONTEXT((#24944))
GLOBAL_UNIT_ASSIGNED_CONTEXT((#25101,#25103,#25104))
REPRESENTATION_CONTEXT('','3D')
);
#25100=(
GEOMETRIC_REPRESENTATION_CONTEXT(3)
GLOBAL_UNCERTAINTY_ASSIGNED_CONTEXT((#24979))
GLOBAL_UNIT_ASSIGNED_CONTEXT((#25101,#25103,#25104))
REPRESENTATION_CONTEXT('','3D')
);
#25101=(
LENGTH_UNIT()
NAMED_UNIT(*)
SI_UNIT(.CENTI.,.METRE.)
);
#25103=(
NAMED_UNIT(*)
PLANE_ANGLE_UNIT()
SI_UNIT($,.RADIAN.)
);
#25104=(
NAMED_UNIT(*)
SI_UNIT($,.STERADIAN.)
SOLID_ANGLE_UNIT()
);
#25190=SHAPE_DEFINITION_REPRESENTATION(#25384,#25595);
#25384=PRODUCT_DEFINITION_SHAPE('',$,#25716);
#25595=SHAPE_REPRESENTATION('',(#15851),#25065);
#25630=PRODUCT_DEFINITION_CONTEXT('part definition',#25992,'design');
#25716=PRODUCT_DEFINITION('M4 low-profile retaining screw',
'M4 low-profile retaining screw',#25836,#25630);
#25836=PRODUCT_DEFINITION_FORMATION('',$,#26079);
#25992=APPLICATION_CONTEXT(
'Core Data for Automotive Mechanical Design Process');
#25993=PRODUCT_CONTEXT('part definition',#25992,'mechanical');
#26079=PRODUCT('M4 low-profile retaining screw',
'M4 low-profile retaining screw','M4 low-profile retaining screw',(#25993));
#26192=COLOUR_RGB('Black',0.12,0.14,0.17);
#26193=FILL_AREA_STYLE_COLOUR('',#26192);
#26194=FILL_AREA_STYLE('',(#26193));
#26195=SURFACE_STYLE_FILL_AREA(#26194);
#26196=SURFACE_SIDE_STYLE('',(#26195));
#26197=SURFACE_STYLE_USAGE(.BOTH.,#26196);
#26198=PRESENTATION_STYLE_ASSIGNMENT((#26197));
ENDSEC;
END-ISO-10303-21;
